ISO-10303-21;
HEADER;
/* Generated by software containing ST-Developer
 * from STEP Tools, Inc. (www.steptools.com) 
 */

FILE_DESCRIPTION(
/* description */ ('Lever-operated bar clamp (toggle)'),
/* implementation_level */ '2;1');

FILE_NAME(
/* name */ 'M4x4 collar screw.step',
/* time_stamp */ '2026-10-28T03:25:02-07:00',
/* author */ (''),
/* organization */ (''),
/* preprocessor_version */ 'ST-DEVELOPER v20.2',
/* originating_system */ 'Autodesk Translation Framework v15.17.0.0',
/* authorisation */ '');

FILE_SCHEMA (('AUTOMOTIVE_DESIGN { 1 0 10303 214 3 1 1 }'));
ENDSEC;

DATA;
#10=MECHANICAL_DESIGN_GEOMETRIC_PRESENTATION_REPRESENTATION('',(#446),#12413);
#316=CONICAL_SURFACE('',#7675,0.185,0.785398163397449);
#362=SHAPE_REPRESENTATION_RELATIONSHIP('SRR','None',#12604,#400);
#400=ADVANCED_BREP_SHAPE_REPRESENTATION('',(#491),#12401);
#446=STYLED_ITEM('',(#12876),#491);
#491=MANIFOLD_SOLID_BREP('Body1',#6607);
#633=FACE_BOUND('',#1738,.T.);
#816=PLANE('',#7664);
#817=PLANE('',#7666);
#818=PLANE('',#7667);
#819=PLANE('',#7668);
#820=PLANE('',#7669);
#821=PLANE('',#7670);
#822=PLANE('',#7671);
#823=PLANE('',#7672);
#824=PLANE('',#7673);
#1190=FACE_OUTER_BOUND('',#1729,.T.);
#1191=FACE_OUTER_BOUND('',#1730,.T.);
#1192=FACE_OUTER_BOUND('',#1731,.T.);
#1193=FACE_OUTER_BOUND('',#1732,.T.);
#1194=FACE_OUTER_BOUND('',#1733,.T.);
#1195=FACE_OUTER_BOUND('',#1734,.T.);
#1196=FACE_OUTER_BOUND('',#1735,.T.);
#1197=FACE_OUTER_BOUND('',#1736,.T.);
#1198=FACE_OUTER_BOUND('',#1737,.T.);
#1199=FACE_OUTER_BOUND('',#1739,.T.);
#1200=FACE_OUTER_BOUND('',#1740,.T.);
#1729=EDGE_LOOP('',(#5623));
#1730=EDGE_LOOP('',(#5624,#5625,#5626,#5627));
#1731=EDGE_LOOP('',(#5628,#5629,#5630,#5631));
#1732=EDGE_LOOP('',(#5632,#5633,#5634,#5635));
#1733=EDGE_LOOP('',(#5636,#5637,#5638,#5639));
#1734=EDGE_LOOP('',(#5640,#5641,#5642,#5643));
#1735=EDGE_LOOP('',(#5644,#5645,#5646,#5647));
#1736=EDGE_LOOP('',(#5648,#5649,#5650,#5651,#5652,#5653));
#1737=EDGE_LOOP('',(#5654));
#1738=EDGE_LOOP('',(#5655,#5656,#5657,#5658,#5659,#5660));
#1739=EDGE_LOOP('',(#5661,#5662,#5663,#5664));
#1740=EDGE_LOOP('',(#5665,#5666,#5667,#5668));
#2148=LINE('',#11801,#2589);
#2149=LINE('',#11803,#2590);
#2150=LINE('',#11805,#2591);
#2151=LINE('',#11806,#2592);
#2152=LINE('',#11809,#2593);
#2153=LINE('',#11811,#2594);
#2154=LINE('',#11812,#2595);
#2155=LINE('',#11815,#2596);
#2156=LINE('',#11817,#2597);
#2157=LINE('',#11818,#2598);
#2158=LINE('',#11821,#2599);
#2159=LINE('',#11823,#2600);
#2160=LINE('',#11824,#2601);
#2161=LINE('',#11827,#2602);
#2162=LINE('',#11829,#2603);
#2163=LINE('',#11830,#2604);
#2164=LINE('',#11832,#2605);
#2165=LINE('',#11833,#2606);
#2166=LINE('',#11841,#2607);
#2167=LINE('',#11843,#2608);
#2589=VECTOR('',#9447,1.);
#2590=VECTOR('',#9448,1.);
#2591=VECTOR('',#9449,1.);
#2592=VECTOR('',#9450,1.);
#2593=VECTOR('',#9453,1.);
#2594=VECTOR('',#9454,1.);
#2595=VECTOR('',#9455,1.);
#2596=VECTOR('',#9458,1.);
#2597=VECTOR('',#9459,1.);
#2598=VECTOR('',#9460,1.);
#2599=VECTOR('',#9463,1.);
#2600=VECTOR('',#9464,1.);
#2601=VECTOR('',#9465,1.);
#2602=VECTOR('',#9468,1.);
#2603=VECTOR('',#9469,1.);
#2604=VECTOR('',#9470,1.);
#2605=VECTOR('',#9473,1.);
#2606=VECTOR('',#9474,1.);
#2607=VECTOR('',#9485,0.185);
#2608=VECTOR('',#9488,0.2);
#3015=CIRCLE('',#7665,0.1954);
#3016=CIRCLE('',#7674,0.17);
#3017=CIRCLE('',#7676,0.1954);
#3482=VERTEX_POINT('',#11796);
#3483=VERTEX_POINT('',#11799);
#3484=VERTEX_POINT('',#11800);
#3485=VERTEX_POINT('',#11802);
#3486=VERTEX_POINT('',#11804);
#3487=VERTEX_POINT('',#11808);
#3488=VERTEX_POINT('',#11810);
#3489=VERTEX_POINT('',#11814);
#3490=VERTEX_POINT('',#11816);
#3491=VERTEX_POINT('',#11820);
#3492=VERTEX_POINT('',#11822);
#3493=VERTEX_POINT('',#11826);
#3494=VERTEX_POINT('',#11828);
#3495=VERTEX_POINT('',#11836);
#3496=VERTEX_POINT('',#11839);
#4216=EDGE_CURVE('',#3482,#3482,#3015,.T.);
#4217=EDGE_CURVE('',#3483,#3484,#2148,.T.);
#4218=EDGE_CURVE('',#3483,#3485,#2149,.T.);
#4219=EDGE_CURVE('',#3485,#3486,#2150,.T.);
#4220=EDGE_CURVE('',#3484,#3486,#2151,.T.);
#4221=EDGE_CURVE('',#3487,#3483,#2152,.T.);
#4222=EDGE_CURVE('',#3487,#3488,#2153,.T.);
#4223=EDGE_CURVE('',#3488,#3485,#2154,.T.);
#4224=EDGE_CURVE('',#3489,#3487,#2155,.T.);
#4225=EDGE_CURVE('',#3489,#3490,#2156,.T.);
#4226=EDGE_CURVE('',#3490,#3488,#2157,.T.);
#4227=EDGE_CURVE('',#3491,#3489,#2158,.T.);
#4228=EDGE_CURVE('',#3491,#3492,#2159,.T.);
#4229=EDGE_CURVE('',#3492,#3490,#2160,.T.);
#4230=EDGE_CURVE('',#3493,#3491,#2161,.T.);
#4231=EDGE_CURVE('',#3493,#3494,#2162,.T.);
#4232=EDGE_CURVE('',#3494,#3492,#2163,.T.);
#4233=EDGE_CURVE('',#3484,#3493,#2164,.T.);
#4234=EDGE_CURVE('',#3486,#3494,#2165,.T.);
#4235=EDGE_CURVE('',#3495,#3495,#3016,.T.);
#4236=EDGE_CURVE('',#3496,#3496,#3017,.T.);
#4237=EDGE_CURVE('',#3496,#3495,#2166,.T.);
#4238=EDGE_CURVE('',#3482,#3496,#2167,.T.);
#5623=ORIENTED_EDGE('',*,*,#4216,.F.);
#5624=ORIENTED_EDGE('',*,*,#4217,.F.);
#5625=ORIENTED_EDGE('',*,*,#4218,.T.);
#5626=ORIENTED_EDGE('',*,*,#4219,.T.);
#5627=ORIENTED_EDGE('',*,*,#4220,.F.);
#5628=ORIENTED_EDGE('',*,*,#4221,.F.);
#5629=ORIENTED_EDGE('',*,*,#4222,.T.);
#5630=ORIENTED_EDGE('',*,*,#4223,.T.);
#5631=ORIENTED_EDGE('',*,*,#4218,.F.);
#5632=ORIENTED_EDGE('',*,*,#4224,.F.);
#5633=ORIENTED_EDGE('',*,*,#4225,.T.);
#5634=ORIENTED_EDGE('',*,*,#4226,.T.);
#5635=ORIENTED_EDGE('',*,*,#4222,.F.);
#5636=ORIENTED_EDGE('',*,*,#4227,.F.);
#5637=ORIENTED_EDGE('',*,*,#4228,.T.);
#5638=ORIENTED_EDGE('',*,*,#4229,.T.);
#5639=ORIENTED_EDGE('',*,*,#4225,.F.);
#5640=ORIENTED_EDGE('',*,*,#4230,.F.);
#5641=ORIENTED_EDGE('',*,*,#4231,.T.);
#5642=ORIENTED_EDGE('',*,*,#4232,.T.);
#5643=ORIENTED_EDGE('',*,*,#4228,.F.);
#5644=ORIENTED_EDGE('',*,*,#4233,.F.);
#5645=ORIENTED_EDGE('',*,*,#4220,.T.);
#5646=ORIENTED_EDGE('',*,*,#4234,.T.);
#5647=ORIENTED_EDGE('',*,*,#4231,.F.);
#5648=ORIENTED_EDGE('',*,*,#4234,.F.);
#5649=ORIENTED_EDGE('',*,*,#4219,.F.);
#5650=ORIENTED_EDGE('',*,*,#4223,.F.);
#5651=ORIENTED_EDGE('',*,*,#4226,.F.);
#5652=ORIENTED_EDGE('',*,*,#4229,.F.);
#5653=ORIENTED_EDGE('',*,*,#4232,.F.);
#5654=ORIENTED_EDGE('',*,*,#4235,.F.);
#5655=ORIENTED_EDGE('',*,*,#4217,.T.);
#5656=ORIENTED_EDGE('',*,*,#4233,.T.);
#5657=ORIENTED_EDGE('',*,*,#4230,.T.);
#5658=ORIENTED_EDGE('',*,*,#4227,.T.);
#5659=ORIENTED_EDGE('',*,*,#4224,.T.);
#5660=ORIENTED_EDGE('',*,*,#4221,.T.);
#5661=ORIENTED_EDGE('',*,*,#4236,.F.);
#5662=ORIENTED_EDGE('',*,*,#4237,.T.);
#5663=ORIENTED_EDGE('',*,*,#4235,.T.);
#5664=ORIENTED_EDGE('',*,*,#4237,.F.);
#5665=ORIENTED_EDGE('',*,*,#4216,.T.);
#5666=ORIENTED_EDGE('',*,*,#4238,.T.);
#5667=ORIENTED_EDGE('',*,*,#4236,.T.);
#5668=ORIENTED_EDGE('',*,*,#4238,.F.);
#6141=CYLINDRICAL_SURFACE('',#7677,0.1954);
#6465=ADVANCED_FACE('',(#1190),#816,.F.);
#6466=ADVANCED_FACE('',(#1191),#817,.F.);
#6467=ADVANCED_FACE('',(#1192),#818,.F.);
#6468=ADVANCED_FACE('',(#1193),#819,.F.);
#6469=ADVANCED_FACE('',(#1194),#820,.F.);
#6470=ADVANCED_FACE('',(#1195),#821,.F.);
#6471=ADVANCED_FACE('',(#1196),#822,.F.);
#6472=ADVANCED_FACE('',(#1197),#823,.F.);
#6473=ADVANCED_FACE('',(#1198,#633),#824,.T.);
#6474=ADVANCED_FACE('',(#1199),#316,.T.);
#6475=ADVANCED_FACE('',(#1200),#6141,.T.);
#6607=CLOSED_SHELL('',(#6465,#6466,#6467,#6468,#6469,#6470,#6471,#6472,
#6473,#6474,#6475));
#7663=AXIS2_PLACEMENT_3D('',#11794,#9439,#9440);
#7664=AXIS2_PLACEMENT_3D('',#11795,#9441,#9442);
#7665=AXIS2_PLACEMENT_3D('',#11797,#9443,#9444);
#7666=AXIS2_PLACEMENT_3D('',#11798,#9445,#9446);
#7667=AXIS2_PLACEMENT_3D('',#11807,#9451,#9452);
#7668=AXIS2_PLACEMENT_3D('',#11813,#9456,#9457);
#7669=AXIS2_PLACEMENT_3D('',#11819,#9461,#9462);
#7670=AXIS2_PLACEMENT_3D('',#11825,#9466,#9467);
#7671=AXIS2_PLACEMENT_3D('',#11831,#9471,#9472);
#7672=AXIS2_PLACEMENT_3D('',#11834,#9475,#9476);
#7673=AXIS2_PLACEMENT_3D('',#11835,#9477,#9478);
#7674=AXIS2_PLACEMENT_3D('',#11837,#9479,#9480);
#7675=AXIS2_PLACEMENT_3D('',#11838,#9481,#9482);
#7676=AXIS2_PLACEMENT_3D('',#11840,#9483,#9484);
#7677=AXIS2_PLACEMENT_3D('',#11842,#9486,#9487);
#9439=DIRECTION('axis',(0.,0.,1.));
#9440=DIRECTION('refdir',(1.,0.,0.));
#9441=DIRECTION('center_axis',(0.,1.,0.));
#9442=DIRECTION('ref_axis',(1.,0.,0.));
#9443=DIRECTION('center_axis',(0.,1.,0.));
#9444=DIRECTION('ref_axis',(1.,0.,0.));
#9445=DIRECTION('center_axis',(0.866025403784439,0.,-0.5));
#9446=DIRECTION('ref_axis',(0.5,0.,0.866025403784439));
#9447=DIRECTION('',(0.5,0.,0.866025403784439));
#9448=DIRECTION('',(0.,-1.,0.));
#9449=DIRECTION('',(0.5,0.,0.866025403784439));
#9450=DIRECTION('',(0.,-1.,0.));
#9451=DIRECTION('center_axis',(1.20185167898973E-16,0.,-1.));
#9452=DIRECTION('ref_axis',(1.,0.,1.20185167898973E-16));
#9453=DIRECTION('',(1.,0.,1.20185167898973E-16));
#9454=DIRECTION('',(0.,-1.,0.));
#9455=DIRECTION('',(1.,0.,1.20185167898973E-16));
#9456=DIRECTION('center_axis',(-0.866025403784439,0.,-0.5));
#9457=DIRECTION('ref_axis',(0.5,0.,-0.866025403784439));
#9458=DIRECTION('',(0.5,0.,-0.866025403784439));
#9459=DIRECTION('',(0.,-1.,0.));
#9460=DIRECTION('',(0.5,0.,-0.866025403784439));
#9461=DIRECTION('center_axis',(-0.866025403784439,0.,0.5));
#9462=DIRECTION('ref_axis',(-0.5,0.,-0.866025403784439));
#9463=DIRECTION('',(-0.5,0.,-0.866025403784439));
#9464=DIRECTION('',(0.,-1.,0.));
#9465=DIRECTION('',(-0.5,0.,-0.866025403784439));
#9466=DIRECTION('center_axis',(-2.40370335797945E-16,0.,1.));
#9467=DIRECTION('ref_axis',(-1.,0.,-2.40370335797945E-16));
#9468=DIRECTION('',(-1.,0.,-2.40370335797945E-16));
#9469=DIRECTION('',(0.,-1.,0.));
#9470=DIRECTION('',(-1.,0.,-2.40370335797945E-16));
#9471=DIRECTION('center_axis',(0.866025403784439,0.,0.5));
#9472=DIRECTION('ref_axis',(-0.5,0.,0.866025403784439));
#9473=DIRECTION('',(-0.5,0.,0.866025403784439));
#9474=DIRECTION('',(-0.5,0.,0.866025403784439));
#9475=DIRECTION('center_axis',(0.,-1.,0.));
#9476=DIRECTION('ref_axis',(0.,0.,-1.));
#9477=DIRECTION('center_axis',(0.,1.,0.));
#9478=DIRECTION('ref_axis',(0.,0.,1.));
#9479=DIRECTION('center_axis',(0.,-1.,0.));
#9480=DIRECTION('ref_axis',(1.,0.,0.));
#9481=DIRECTION('center_axis',(0.,-1.,0.));
#9482=DIRECTION('ref_axis',(1.,0.,0.));
#9483=DIRECTION('center_axis',(0.,-1.,0.));
#9484=DIRECTION('ref_axis',(1.,0.,0.));
#9485=DIRECTION('',(0.707106781186548,0.707106781186547,8.65956056235494E-17));
#9486=DIRECTION('center_axis',(0.,-1.,0.));
#9487=DIRECTION('ref_axis',(1.,0.,0.));
#9488=DIRECTION('',(0.,1.,0.));
#11794=CARTESIAN_POINT('',(0.,0.,0.));
#11795=CARTESIAN_POINT('Origin',(0.,-0.4,0.));
#11796=CARTESIAN_POINT('',(-0.1954,-0.4,2.39295984553393E-17));
#11797=CARTESIAN_POINT('Origin',(0.,-0.4,0.));
#11798=CARTESIAN_POINT('Origin',(0.0577350269189626,0.,-0.1));
#11799=CARTESIAN_POINT('',(0.0577350269189626,0.,-0.1));
#11800=CARTESIAN_POINT('',(0.115470053837925,0.,0.));
#11801=CARTESIAN_POINT('',(0.0934187836487032,0.,-0.0381939203391614));
#11802=CARTESIAN_POINT('',(0.0577350269189626,-0.2,-0.1));
#11803=CARTESIAN_POINT('',(0.0577350269189626,0.,-0.1));
#11804=CARTESIAN_POINT('',(0.115470053837925,-0.2,0.));
#11805=CARTESIAN_POINT('',(0.115470053837925,-0.2,0.));
#11806=CARTESIAN_POINT('',(0.115470053837925,0.,0.));
#11807=CARTESIAN_POINT('Origin',(-0.0577350269189626,0.,-0.1));
#11808=CARTESIAN_POINT('',(-0.0577350269189626,0.,-0.1));
#11809=CARTESIAN_POINT('',(0.0561324865405187,0.,-0.1));
#11810=CARTESIAN_POINT('',(-0.0577350269189626,-0.2,-0.1));
#11811=CARTESIAN_POINT('',(-0.0577350269189626,0.,-0.1));
#11812=CARTESIAN_POINT('',(0.0577350269189626,-0.2,-0.1));
#11813=CARTESIAN_POINT('Origin',(-0.115470053837925,0.,-1.38777878078145E-17));
#11814=CARTESIAN_POINT('',(-0.115470053837925,0.,-1.41410031829988E-17));
#11815=CARTESIAN_POINT('',(-0.0797862971081845,0.,-0.0618060796608387));
#11816=CARTESIAN_POINT('',(-0.115470053837925,-0.2,-1.38777878078145E-17));
#11817=CARTESIAN_POINT('',(-0.115470053837925,0.,-1.41410031829988E-17));
#11818=CARTESIAN_POINT('',(-0.0577350269189626,-0.2,-0.1));
#11819=CARTESIAN_POINT('Origin',(-0.0577350269189626,0.,0.1));
#11820=CARTESIAN_POINT('',(-0.0577350269189626,0.,0.1));
#11821=CARTESIAN_POINT('',(-0.0509187836487033,0.,0.111806079660839));
#11822=CARTESIAN_POINT('',(-0.0577350269189626,-0.2,0.1));
#11823=CARTESIAN_POINT('',(-0.0577350269189626,0.,0.1));
#11824=CARTESIAN_POINT('',(-0.115470053837925,-0.2,-1.41410031829988E-17));
#11825=CARTESIAN_POINT('Origin',(0.0577350269189626,0.,0.1));
#11826=CARTESIAN_POINT('',(0.0577350269189626,0.,0.1));
#11827=CARTESIAN_POINT('',(0.113867513459481,0.,0.1));
#11828=CARTESIAN_POINT('',(0.0577350269189626,-0.2,0.1));
#11829=CARTESIAN_POINT('',(0.0577350269189626,0.,0.1));
#11830=CARTESIAN_POINT('',(-0.0577350269189626,-0.2,0.1));
#11831=CARTESIAN_POINT('Origin',(0.115470053837925,0.,0.));
#11832=CARTESIAN_POINT('',(0.122286297108185,0.,-0.0118060796608386));
#11833=CARTESIAN_POINT('',(0.0577350269189626,-0.2,0.1));
#11834=CARTESIAN_POINT('Origin',(0.,-0.2,0.));
#11835=CARTESIAN_POINT('Origin',(0.17,0.,0.));
#11836=CARTESIAN_POINT('',(-0.17,-8.67361737988404E-18,-2.0818995585505E-17));
#11837=CARTESIAN_POINT('Origin',(0.,0.,0.));
#11838=CARTESIAN_POINT('Origin',(0.,-0.015,0.));
#11839=CARTESIAN_POINT('',(-0.1954,-0.0254,-2.39295984553393E-17));
#11840=CARTESIAN_POINT('Origin',(0.,-0.0254,0.));
#11841=CARTESIAN_POINT('',(-0.185,-0.015,-2.2655965784226E-17));
#11842=CARTESIAN_POINT('Origin',(0.,-0.2775,0.));
#11843=CARTESIAN_POINT('',(-0.1954,-0.2775,-2.39295984553393E-17));
#12355=UNCERTAINTY_MEASURE_WITH_UNIT(LENGTH_MEASURE(0.001),#12414,
'DISTANCE_ACCURACY_VALUE',
'Maximum model space distance between geometric entities at asserted c
onnectivities');
#12367=UNCERTAINTY_MEASURE_WITH_UNIT(LENGTH_MEASURE(0.001),#12414,
'DISTANCE_ACCURACY_VALUE',
'Maximum model space distance between geometric entities at asserted c
onnectivities');
#12401=(
GEOMETRIC_REPRESENTATION_CONTEXT(3)
GLOBAL_UNCERTAINTY_ASSIGNED_CONTEXT((#12355))
GLOBAL_UNIT_ASSIGNED_CONTEXT((#12414,#12416,#12417))
REPRESENTATION_CONTEXT('','3D')
);
#12413=(
GEOMETRIC_REPRESENTATION_CONTEXT(3)
GLOBAL_UNCERTAINTY_ASSIGNED_CONTEXT((#12367))
GLOBAL_UNIT_ASSIGNED_CONTEXT((#12414,#12416,#12417))
REPRESENTATION_CONTEXT('','3D')
);
#12414=(
LENGTH_UNIT()
NAMED_UNIT(*)
SI_UNIT(.CENTI.,.METRE.)
);
#12416=(
NAMED_UNIT(*)
PLANE_ANGLE_UNIT()
SI_UNIT($,.RADIAN.)
);
#12417=(
NAMED_UNIT(*)
SI_UNIT($,.STERADIAN.)
SOLID_ANGLE_UNIT()
);
#12451=SHAPE_DEFINITION_REPRESENTATION(#12503,#12604);
#12503=PRODUCT_DEFINITION_SHAPE('',$,#12650);
#12604=SHAPE_REPRESENTATION('',(#7663),#12401);
#12616=PRODUCT_DEFINITION_CONTEXT('part definition',#12753,'design');
#12650=PRODUCT_DEFINITION('M4x4 collar screw','M4x4 collar screw',#12695,
#12616);
#12695=PRODUCT_DEFINITION_FORMATION('',$,#12788);
#12753=APPLICATION_CONTEXT(
'Core Data for Automotive Mechanical Design Process');
#12754=PRODUCT_CONTEXT('part definition',#12753,'mechanical');
#12788=PRODUCT('M4x4 collar screw','M4x4 collar screw',
'M4x4 collar screw',(#12754));
#12870=COLOUR_RGB('Black',0.12,0.14,0.17);
#12871=FILL_AREA_STYLE_COLOUR('',#12870);
#12872=FILL_AREA_STYLE('',(#12871));
#12873=SURFACE_STYLE_FILL_AREA(#12872);
#12874=SURFACE_SIDE_STYLE('',(#12873));
#12875=SURFACE_STYLE_USAGE(.BOTH.,#12874);
#12876=PRESENTATION_STYLE_ASSIGNMENT((#12875));
ENDSEC;
END-ISO-10303-21;
